ISO-10303-21;
HEADER;
FILE_DESCRIPTION (('STEP AP214'),
    '1' );
FILE_NAME ('socket head cap screw_iso_ISO 4762 M8 x 70 - 28N.step',
    '2026-10-08T07:58:12',
    ( '' ),
    ( '' ),
    'SwSTEP 2.0',
    'SolidWorks 2026',
    '' );
FILE_SCHEMA (( 'AUTOMOTIVE_DESIGN' ));
ENDSEC;

DATA;
#1=EDGE_CURVE ( 'NONE', #21367, #4979, #7430, .T. ) ;
#37=PLANE ( 'NONE',  #25790 ) ;
#259=CARTESIAN_POINT ( 'NONE',  ( 4.000000000000000000, 3.518949890710768802, -4.770489558936219510E-15 ) ) ;
#373=FACE_OUTER_BOUND ( 'NONE', #11507, .T. ) ;
#413=FACE_OUTER_BOUND ( 'NONE', #6804, .T. ) ;
#525=CARTESIAN_POINT ( 'NONE',  ( 4.000000000000000000, 1.759474945355380404, -3.047500000000001652 ) ) ;
#682=DIRECTION ( 'NONE',  ( 0.000000000000000000, -1.000000000000000000, 0.000000000000000000 ) ) ;
#691=ORIENTED_EDGE ( 'NONE', *, *, #18686, .T. ) ;
#756=DIRECTION ( 'NONE',  ( -1.000000000000000000, -0.000000000000000000, -0.000000000000000000 ) ) ;
#780=VERTEX_POINT ( 'NONE', #29440 ) ;
#783=EDGE_LOOP ( 'NONE', ( #26414, #22482, #29062, #10811 ) ) ;
#814=EDGE_CURVE ( 'NONE', #4673, #6298, #27597, .T. ) ;
#864=LINE ( 'NONE', #21144, #15127 ) ;
#955=VECTOR ( 'NONE', #756, 1000.000000000000000 ) ;
#987=EDGE_LOOP ( 'NONE', ( #4854, #13147, #24836, #25299, #30659 ) ) ;
#1000=EDGE_CURVE ( 'NONE', #5337, #6298, #8048, .T. ) ;
#1047=FACE_OUTER_BOUND ( 'NONE', #1653, .T. ) ;
#1063=EDGE_CURVE ( 'NONE', #15562, #30489, #11824, .T. ) ;
#1078=EDGE_LOOP ( 'NONE', ( #2639, #30744, #24589, #33121 ) ) ;
#1122=EDGE_LOOP ( 'NONE', ( #25752, #2521, #18480, #9209 ) ) ;
#1139=EDGE_CURVE ( 'NONE', #15105, #26666, #12565, .T. ) ;
#1169=VECTOR ( 'NONE', #26440, 1000.000000000000000 ) ;
#1206=DIRECTION ( 'NONE',  ( 0.000000000000000000, 0.4999999999999990563, -0.8660254037844391517 ) ) ;
#1223=ORIENTED_EDGE ( 'NONE', *, *, #17026, .F. ) ;
#1363=ORIENTED_EDGE ( 'NONE', *, *, #31628, .F. ) ;
#1427=DIRECTION ( 'NONE',  ( 0.000000000000000000, 1.000000000000000000, -1.478898702612462246E-15 ) ) ;
#1451=DIRECTION ( 'NONE',  ( 0.000000000000000000, -0.4999999999999995004, 0.8660254037844389297 ) ) ;
#1498=DIRECTION ( 'NONE',  ( 0.000000000000000000, 0.000000000000000000, -1.000000000000000000 ) ) ;
#1531=EDGE_LOOP ( 'NONE', ( #25675, #4715, #28812, #32881 ) ) ;
#1554=CARTESIAN_POINT ( 'NONE',  ( 8.399999999999998579, 0.000000000000000000, 4.000000000000000888 ) ) ;
#1560=CIRCLE ( 'NONE', #7565, 6.500000000000000000 ) ;
#1582=CARTESIAN_POINT ( 'NONE',  ( 8.399999999999998579, 0.000000000000000000, 0.000000000000000000 ) ) ;
#1583=EDGE_LOOP ( 'NONE', ( #28454, #13185, #30058, #28016 ) ) ;
#1648=ORIENTED_EDGE ( 'NONE', *, *, #25576, .T. ) ;
#1653=EDGE_LOOP ( 'NONE', ( #9933, #8897, #9960 ) ) ;
#1667=DIRECTION ( 'NONE',  ( -1.000000000000000000, -0.000000000000000000, -0.000000000000000000 ) ) ;
#1719=DIRECTION ( 'NONE',  ( 0.000000000000000000, 0.000000000000000000, 1.000000000000000000 ) ) ;
#1764=ORIENTED_EDGE ( 'NONE', *, *, #27471, .F. ) ;
#1786=CARTESIAN_POINT ( 'NONE',  ( 4.000000000000000000, -1.759474945355388176, -3.047499999999998099 ) ) ;
#1820=CARTESIAN_POINT ( 'NONE',  ( 4.000000000000000000, 0.000000000000000000, 0.000000000000000000 ) ) ;
#1826=EDGE_CURVE ( 'NONE', #26666, #33208, #33149, .T. ) ;
#1843=AXIS2_PLACEMENT_3D ( 'NONE', #19421, #29826, #6487 ) ;
#1984=VECTOR ( 'NONE', #1667, 1000.000000000000000 ) ;
#1992=EDGE_CURVE ( 'NONE', #2597, #15105, #31874, .T. ) ;
#2071=EDGE_CURVE ( 'NONE', #30105, #15562, #25515, .T. ) ;
#2244=DIRECTION ( 'NONE',  ( 0.000000000000000000, 0.000000000000000000, 1.000000000000000000 ) ) ;
#2261=EDGE_CURVE ( 'NONE', #27176, #32104, #10074, .T. ) ;
#2304=FACE_OUTER_BOUND ( 'NONE', #1531, .T. ) ;
#2353=VECTOR ( 'NONE', #21963, 1000.000000000000000 ) ;
#2404=AXIS2_PLACEMENT_3D ( 'NONE', #8872, #11941, #4266 ) ;
#2453=CARTESIAN_POINT ( 'NONE',  ( 4.000000000000000000, -3.004629197474319246E-15, -3.047499999999999876 ) ) ;
#2502=LINE ( 'NONE', #15937, #15920 ) ;
#2521=ORIENTED_EDGE ( 'NONE', *, *, #814, .T. ) ;
#2556=DIRECTION ( 'NONE',  ( -1.000000000000000000, -0.000000000000000000, -0.000000000000000000 ) ) ;
#2588=VERTEX_POINT ( 'NONE', #23507 ) ;
#2597=VERTEX_POINT ( 'NONE', #7515 ) ;
#2628=EDGE_LOOP ( 'NONE', ( #28820, #26747, #6296, #23074, #16613, #15198 ) ) ;
#2639=ORIENTED_EDGE ( 'NONE', *, *, #25144, .T. ) ;
#2684=DIRECTION ( 'NONE',  ( -1.000000000000000000, -0.000000000000000000, -0.000000000000000000 ) ) ;
#2699=DIRECTION ( 'NONE',  ( 0.000000000000000000, 1.000000000000000000, -9.859324684083082301E-16 ) ) ;
#2810=FACE_BOUND ( 'NONE', #27161, .T. ) ;
#2832=FACE_OUTER_BOUND ( 'NONE', #25921, .T. ) ;
#2844=DIRECTION ( 'NONE',  ( 1.000000000000000000, 0.000000000000000000, 0.000000000000000000 ) ) ;
#2854=DIRECTION ( 'NONE',  ( -0.5000000000000061062, 0.000000000000000000, 0.8660254037844351549 ) ) ;
#2904=DIRECTION ( 'NONE',  ( 0.000000000000000000, -0.5000000000000013323, -0.8660254037844379305 ) ) ;
#2917=ORIENTED_EDGE ( 'NONE', *, *, #1, .T. ) ;
#2928=AXIS2_PLACEMENT_3D ( 'NONE', #11132, #27792, #4457 ) ;
#2955=EDGE_CURVE ( 'NONE', #30489, #15562, #3291, .T. ) ;
#2967=CARTESIAN_POINT ( 'NONE',  ( 0.3999999999999975797, 0.000000000000000000, 6.500000000000000000 ) ) ;
#3038=ORIENTED_EDGE ( 'NONE', *, *, #2261, .F. ) ;
#3071=AXIS2_PLACEMENT_3D ( 'NONE', #32779, #32953, #27674 ) ;
#3087=ORIENTED_EDGE ( 'NONE', *, *, #23945, .F. ) ;
#3222=DIRECTION ( 'NONE',  ( 0.000000000000000000, 0.000000000000000000, 1.000000000000000000 ) ) ;
#3235=CARTESIAN_POINT ( 'NONE',  ( 0.3999999999999975797, 0.000000000000000000, 6.099999999999999645 ) ) ;
#3248=DIRECTION ( 'NONE',  ( -1.000000000000000000, -0.000000000000000000, -0.000000000000000000 ) ) ;
#3291=CIRCLE ( 'NONE', #14188, 6.099999999999999645 ) ;
#3295=PLANE ( 'NONE',  #6420 ) ;
#3313=CARTESIAN_POINT ( 'NONE',  ( 4.000000000000000000, 0.000000000000000000, 0.000000000000000000 ) ) ;
#3374=CARTESIAN_POINT ( 'NONE',  ( 8.399999999999998579, 5.388445916248354999E-16, 4.400000000000001243 ) ) ;
#3457=STYLED_ITEM ( 'NONE', ( #27352 ), #33198 ) ;
#3496=ORIENTED_EDGE ( 'NONE', *, *, #6032, .T. ) ;
#3530=FILL_AREA_STYLE ('',( #9315 ) ) ;
#3561=CARTESIAN_POINT ( 'NONE',  ( 0.000000000000000000, 3.518949890710768802, -4.770489558936219510E-15 ) ) ;
#3641=MECHANICAL_DESIGN_GEOMETRIC_PRESENTATION_REPRESENTATION('',(#11264),#6367);
#3689=TOROIDAL_SURFACE ( 'NONE', #22746, 6.099999999999999645, 0.4000000000000000222 ) ;
#3702=PRESENTATION_STYLE_ASSIGNMENT (( #6594 ) ) ;
#3768=PLANE ( 'NONE',  #6907 ) ;
#3814=DIRECTION ( 'NONE',  ( 0.000000000000000000, 0.000000000000000000, 1.000000000000000000 ) ) ;
#3911=ORIENTED_EDGE ( 'NONE', *, *, #9591, .F. ) ;
#3913=FACE_OUTER_BOUND ( 'NONE', #13666, .T. ) ;
#3967=DIRECTION ( 'NONE',  ( 0.000000000000000000, -1.000000000000000000, 9.859324684083082301E-16 ) ) ;
#4019=( NAMED_UNIT ( * ) SI_UNIT ( $, .STERADIAN. ) SOLID_ANGLE_UNIT ( ) );
#4024=VECTOR ( 'NONE', #6461, 1000.000000000000000 ) ;
#4054=CARTESIAN_POINT ( 'NONE',  ( 4.000000000000000000, 3.518949890710768802, -4.770489558936219510E-15 ) ) ;
#4085=DIRECTION ( 'NONE',  ( 0.000000000000000000, 0.8660254037844380415, -0.5000000000000009992 ) ) ;
#4119=CARTESIAN_POINT ( 'NONE',  ( -31.74999999999995737, 0.000000000000000000, 0.000000000000000000 ) ) ;
#4170=EDGE_CURVE ( 'NONE', #24055, #10071, #25784, .T. ) ;
#4186=DIRECTION ( 'NONE',  ( -0.7071067811865314745, 0.000000000000000000, 0.7071067811865635599 ) ) ;
#4266=DIRECTION ( 'NONE',  ( 1.000000000000000000, 0.000000000000000000, 0.000000000000000000 ) ) ;
#4292=CONICAL_SURFACE ( 'NONE', #13529, 3.047499999999999876, 1.047197551196590748 ) ;
#4383=ORIENTED_EDGE ( 'NONE', *, *, #32414, .T. ) ;
#4425=FACE_OUTER_BOUND ( 'NONE', #7153, .T. ) ;
#4457=DIRECTION ( 'NONE',  ( 0.000000000000000000, 0.000000000000000000, -1.000000000000000000 ) ) ;
#4508=AXIS2_PLACEMENT_3D ( 'NONE', #3235, #682, #11084 ) ;
#4673=VERTEX_POINT ( 'NONE', #1554 ) ;
#4715=ORIENTED_EDGE ( 'NONE', *, *, #2071, .T. ) ;
#4730=PLANE ( 'NONE',  #16189 ) ;
#4789=ADVANCED_FACE ( 'NONE', ( #6669 ), #14336, .F. ) ;
#4854=ORIENTED_EDGE ( 'NONE', *, *, #30340, .T. ) ;
#4855=APPLICATION_CONTEXT ( 'automotive_design' ) ;
#4877=EDGE_CURVE ( 'NONE', #33593, #5010, #23506, .T. ) ;
#4934=ORIENTED_EDGE ( 'NONE', *, *, #1063, .T. ) ;
#4936=DIRECTION ( 'NONE',  ( 0.000000000000000000, 0.000000000000000000, 1.000000000000000000 ) ) ;
#4974=ORIENTED_EDGE ( 'NONE', *, *, #1, .F. ) ;
#4979=VERTEX_POINT ( 'NONE', #5126 ) ;
#5010=VERTEX_POINT ( 'NONE', #18244 ) ;
#5126=CARTESIAN_POINT ( 'NONE',  ( 4.000000000000000000, 2.639212418033077157, 1.523749999999998161 ) ) ;
#5183=ORIENTED_EDGE ( 'NONE', *, *, #21633, .F. ) ;
#5216=PLANE ( 'NONE',  #32771 ) ;
#5226=ORIENTED_EDGE ( 'NONE', *, *, #26790, .T. ) ;
#5237=DIRECTION ( 'NONE',  ( 0.000000000000000000, 0.5000000000000013323, 0.8660254037844379305 ) ) ;
#5334=AXIS2_PLACEMENT_3D ( 'NONE', #25462, #10141, #20359 ) ;
#5337=VERTEX_POINT ( 'NONE', #23844 ) ;
#5382=VECTOR ( 'NONE', #17641, 1000.000000000000000 ) ;
#5408=FACE_OUTER_BOUND ( 'NONE', #987, .T. ) ;
#5522=PLANE ( 'NONE',  #10534 ) ;
#5596=ADVANCED_FACE ( 'NONE', ( #2304 ), #3689, .T. ) ;
#5599=CARTESIAN_POINT ( 'NONE',  ( 4.000000000000000000, 3.518949890710768802, -4.770489558936219510E-15 ) ) ;
#5611=TOROIDAL_SURFACE ( 'NONE', #6690, 6.099999999999999645, 0.4000000000000000222 ) ;
#5659=VECTOR ( 'NONE', #2904, 1000.000000000000000 ) ;
#5750=VERTEX_POINT ( 'NONE', #20697 ) ;
#5795=CARTESIAN_POINT ( 'NONE',  ( 4.000000000000000000, 0.000000000000000000, 0.000000000000000000 ) ) ;
#5799=ADVANCED_FACE ( 'NONE', ( #2810, #413 ), #3295, .T. ) ;
#5839=ORIENTED_EDGE ( 'NONE', *, *, #1992, .F. ) ;
#5857=LINE ( 'NONE', #14380, #30890 ) ;
#6032=EDGE_CURVE ( 'NONE', #27878, #26666, #27144, .T. ) ;
#6049=EDGE_CURVE ( 'NONE', #4673, #5750, #30358, .T. ) ;
#6115=CARTESIAN_POINT ( 'NONE',  ( 0.3999999999999975797, 0.000000000000000000, 0.000000000000000000 ) ) ;
#6175=EDGE_LOOP ( 'NONE', ( #13013, #3911 ) ) ;
#6222=VERTEX_POINT ( 'NONE', #6862 ) ;
#6254=SURFACE_STYLE_FILL_AREA ( #3530 ) ;
#6296=ORIENTED_EDGE ( 'NONE', *, *, #2261, .T. ) ;
#6298=VERTEX_POINT ( 'NONE', #18367 ) ;
#6346=UNCERTAINTY_MEASURE_WITH_UNIT (LENGTH_MEASURE( 1.000000000000000082E-05 ), #32798, 'distance_accuracy_value', 'NONE');
#6367=( GEOMETRIC_REPRESENTATION_CONTEXT ( 3 ) GLOBAL_UNCERTAINTY_ASSIGNED_CONTEXT ( ( #21558 ) ) GLOBAL_UNIT_ASSIGNED_CONTEXT ( ( #32821, #27538, #27373 ) ) REPRESENTATION_CONTEXT ( 'NONE', 'WORKASPACE' ) );
#6408=( NAMED_UNIT ( * ) PLANE_ANGLE_UNIT ( ) SI_UNIT ( $, .RADIAN. ) );
#6420=AXIS2_PLACEMENT_3D ( 'NONE', #11146, #23590, #13679 ) ;
#6461=DIRECTION ( 'NONE',  ( -1.000000000000000000, -0.000000000000000000, -0.000000000000000000 ) ) ;
#6487=DIRECTION ( 'NONE',  ( 0.000000000000000000, 0.000000000000000000, 1.000000000000000000 ) ) ;
#6517=DIRECTION ( 'NONE',  ( -1.000000000000000000, -0.000000000000000000, -0.000000000000000000 ) ) ;
#6594=SURFACE_STYLE_USAGE ( .BOTH. , #22266 ) ;
#6669=FACE_OUTER_BOUND ( 'NONE', #9323, .T. ) ;
#6690=AXIS2_PLACEMENT_3D ( 'NONE', #20728, #2684, #20900 ) ;
#6723=ORIENTED_EDGE ( 'NONE', *, *, #12014, .F. ) ;
#6804=EDGE_LOOP ( 'NONE', ( #7511, #31697 ) ) ;
#6862=CARTESIAN_POINT ( 'NONE',  ( 5.759474945355412601, 0.000000000000000000, 0.000000000000000000 ) ) ;
#6907=AXIS2_PLACEMENT_3D ( 'NONE', #11602, #9040, #29836 ) ;
#6912=COLOUR_RGB ( '', 0.66274510, 0.83137255, 0.94901961) ;
#6985=VERTEX_POINT ( 'NONE', #18493 ) ;
#6987=PRODUCT_DEFINITION_SHAPE ( 'NONE', 'NONE',  #12945 ) ;
#6997=VECTOR ( 'NONE', #27239, 1000.000000000000000 ) ;
#7041=DIRECTION ( 'NONE',  ( 0.000000000000000000, 0.000000000000000000, 1.000000000000000000 ) ) ;
#7049=EDGE_CURVE ( 'NONE', #27176, #32876, #28877, .T. ) ;
#7153=EDGE_LOOP ( 'NONE', ( #3038, #15070, #18142, #25253, #12131 ) ) ;
#7225=DIRECTION ( 'NONE',  ( 1.000000000000000000, 0.000000000000000000, 0.000000000000000000 ) ) ;
#7229=AXIS2_PLACEMENT_3D ( 'NONE', #25456, #12514, #27834 ) ;
#7303=VECTOR ( 'NONE', #24688, 1000.000000000000114 ) ;
#7345=CARTESIAN_POINT ( 'NONE',  ( 0.000000000000000000, 1.759474945355380404, -3.047500000000001652 ) ) ;
#7430=CIRCLE ( 'NONE', #3071, 3.047499999999999876 ) ;
#7511=ORIENTED_EDGE ( 'NONE', *, *, #16196, .F. ) ;
#7515=CARTESIAN_POINT ( 'NONE',  ( 4.000000000000000000, -3.518949890710769246, 3.686287386450715076E-15 ) ) ;
#7528=PLANE ( 'NONE',  #8592 ) ;
#7537=ORIENTED_EDGE ( 'NONE', *, *, #13328, .F. ) ;
#7565=AXIS2_PLACEMENT_3D ( 'NONE', #15783, #2844, #18518 ) ;
#7686=PRODUCT_CONTEXT ( 'NONE', #29882, 'mechanical' ) ;
#7695=ADVANCED_FACE ( 'NONE', ( #15729 ), #28003, .F. ) ;
#7783=DIRECTION ( 'NONE',  ( 0.000000000000000000, 0.000000000000000000, -1.000000000000000000 ) ) ;
#7802=CARTESIAN_POINT ( 'NONE',  ( 4.000000000000000000, 3.518949890710768802, -4.770489558936219510E-15 ) ) ;
#7839=ORIENTED_EDGE ( 'NONE', *, *, #13501, .T. ) ;
#7875=ORIENTED_EDGE ( 'NONE', *, *, #19865, .T. ) ;
#7970=AXIS2_PLACEMENT_3D ( 'NONE', #27319, #19826, #3814 ) ;
#8048=CIRCLE ( 'NONE', #12361, 4.400000000000001243 ) ;
#8065=LINE ( 'NONE', #21323, #25780 ) ;
#8194=DIRECTION ( 'NONE',  ( 1.000000000000000000, 0.000000000000000000, 0.000000000000000000 ) ) ;
#8308=CARTESIAN_POINT ( 'NONE',  ( 4.000000000000000000, 3.518949890710768802, -4.770489558936219510E-15 ) ) ;
#8566=AXIS2_PLACEMENT_3D ( 'NONE', #1820, #20216, #28051 ) ;
#8592=AXIS2_PLACEMENT_3D ( 'NONE', #26236, #8194, #18579 ) ;
#8669=DIRECTION ( 'NONE',  ( -1.000000000000000000, -0.000000000000000000, -0.000000000000000000 ) ) ;
#8870=DIRECTION ( 'NONE',  ( 0.000000000000000000, 0.000000000000000000, -1.000000000000000000 ) ) ;
#8872=CARTESIAN_POINT ( 'NONE',  ( 0.000000000000000000, 0.000000000000000000, 0.000000000000000000 ) ) ;
#8896=CARTESIAN_POINT ( 'NONE',  ( 4.000000000000000000, 3.518949890710768802, -4.770489558936219510E-15 ) ) ;
#8897=ORIENTED_EDGE ( 'NONE', *, *, #29077, .T. ) ;
#8987=ORIENTED_EDGE ( 'NONE', *, *, #27471, .T. ) ;
#9040=DIRECTION ( 'NONE',  ( 1.000000000000000000, 0.000000000000000000, 0.000000000000000000 ) ) ;
#9076=DIRECTION ( 'NONE',  ( 0.000000000000000000, 0.000000000000000000, -1.000000000000000000 ) ) ;
#9077=CIRCLE ( 'NONE', #11805, 4.400000000000001243 ) ;
#9132=FACE_OUTER_BOUND ( 'NONE', #1078, .T. ) ;
#9169=ORIENTED_EDGE ( 'NONE', *, *, #12946, .F. ) ;
#9171=VECTOR ( 'NONE', #27945, 1000.000000000000000 ) ;
#9179=DIRECTION ( 'NONE',  ( -1.000000000000000000, -0.000000000000000000, -0.000000000000000000 ) ) ;
#9190=CARTESIAN_POINT ( 'NONE',  ( -31.74999999999995737, 0.000000000000000000, 4.000000000000000888 ) ) ;
#9209=ORIENTED_EDGE ( 'NONE', *, *, #16055, .F. ) ;
#9259=ADVANCED_FACE ( 'NONE', ( #11328 ), #32270, .F. ) ;
#9315=FILL_AREA_STYLE_COLOUR ( '', #6912 ) ;
#9323=EDGE_LOOP ( 'NONE', ( #21481, #22685, #6723 ) ) ;
#9335=DIRECTION ( 'NONE',  ( -1.000000000000000000, -0.000000000000000000, -0.000000000000000000 ) ) ;
#9408=FACE_OUTER_BOUND ( 'NONE', #14054, .T. ) ;
#9449=MECHANICAL_DESIGN_GEOMETRIC_PRESENTATION_REPRESENTATION('',(#3457),#23587);
#9499=DIRECTION ( 'NONE',  ( -1.000000000000000000, -0.000000000000000000, -0.000000000000000000 ) ) ;
#9550=ADVANCED_FACE ( 'NONE', ( #1047 ), #3768, .F. ) ;
#9591=EDGE_CURVE ( 'NONE', #2588, #24969, #19424, .T. ) ;
#9622=DIRECTION ( 'NONE',  ( -1.000000000000000000, -0.000000000000000000, -0.000000000000000000 ) ) ;
#9657=VERTEX_POINT ( 'NONE', #25385 ) ;
#9702=ORIENTED_EDGE ( 'NONE', *, *, #24915, .F. ) ;
#9765=CARTESIAN_POINT ( 'NONE',  ( 8.399999999999998579, 0.000000000000000000, 0.000000000000000000 ) ) ;
#9883=CARTESIAN_POINT ( 'NONE',  ( 0.000000000000000000, -3.518949890710769246, 3.686287386450715076E-15 ) ) ;
#9919=ORIENTED_EDGE ( 'NONE', *, *, #1826, .T. ) ;
#9933=ORIENTED_EDGE ( 'NONE', *, *, #26173, .F. ) ;
#9960=ORIENTED_EDGE ( 'NONE', *, *, #28282, .F. ) ;
#9969=LINE ( 'NONE', #23077, #13753 ) ;
#9976=CARTESIAN_POINT ( 'NONE',  ( 8.000000000000000000, 0.000000000000000000, 0.000000000000000000 ) ) ;
#9995=COLOUR_RGB ( '', 0.66274510, 0.83137255, 0.94901961) ;
#10035=AXIS2_PLACEMENT_3D ( 'NONE', #24711, #3248, #21307 ) ;
#10071=VERTEX_POINT ( 'NONE', #7345 ) ;
#10074=LINE ( 'NONE', #19773, #9171 ) ;
#10141=DIRECTION ( 'NONE',  ( -1.000000000000000000, -0.000000000000000000, -0.000000000000000000 ) ) ;
#10149=DIRECTION ( 'NONE',  ( -0.000000000000000000, 0.8660254037844391517, 0.4999999999999990563 ) ) ;
#10275=ORIENTED_EDGE ( 'NONE', *, *, #31628, .T. ) ;
#10481=DIRECTION ( 'NONE',  ( 1.000000000000000000, 0.000000000000000000, 0.000000000000000000 ) ) ;
#10500=ADVANCED_FACE ( 'NONE', ( #33356 ), #4730, .F. ) ;
#10534=AXIS2_PLACEMENT_3D ( 'NONE', #17982, #10149, #30763 ) ;
#10567=CIRCLE ( 'NONE', #1843, 3.047499999999999876 ) ;
#10576=ADVANCED_FACE ( 'NONE', ( #5408 ), #15119, .F. ) ;
#10661=CARTESIAN_POINT ( 'NONE',  ( 0.000000000000000000, -1.759474945355381958, 3.047500000000001208 ) ) ;
#10811=ORIENTED_EDGE ( 'NONE', *, *, #1063, .F. ) ;
#10845=DIRECTION ( 'NONE',  ( 1.000000000000000000, 0.000000000000000000, 0.000000000000000000 ) ) ;
#10917=DIRECTION ( 'NONE',  ( 0.000000000000000000, -1.000000000000000000, 9.859324684083082301E-16 ) ) ;
#10970=FACE_OUTER_BOUND ( 'NONE', #1122, .T. ) ;
#11084=DIRECTION ( 'NONE',  ( 0.000000000000000000, 0.000000000000000000, -1.000000000000000000 ) ) ;
#11112=CARTESIAN_POINT ( 'NONE',  ( 4.000000000000000000, -3.518949890710769246, 3.686287386450715076E-15 ) ) ;
#11132=CARTESIAN_POINT ( 'NONE',  ( 8.399999999999998579, 0.000000000000000000, -4.400000000000001243 ) ) ;
#11146=CARTESIAN_POINT ( 'NONE',  ( 8.000000000000000000, 6.500000000000000000, 0.000000000000000000 ) ) ;
#11264=STYLED_ITEM ( 'NONE', ( #3702 ), #23704 ) ;
#11328=FACE_OUTER_BOUND ( 'NONE', #30582, .T. ) ;
#11353=( NAMED_UNIT ( * ) SI_UNIT ( $, .STERADIAN. ) SOLID_ANGLE_UNIT ( ) );
#11438=DIRECTION ( 'NONE',  ( 1.000000000000000000, 0.000000000000000000, 0.000000000000000000 ) ) ;
#11507=EDGE_LOOP ( 'NONE', ( #24861, #15998, #25044, #30323 ) ) ;
#11602=CARTESIAN_POINT ( 'NONE',  ( 4.000000000000000000, 3.518949890710768802, -4.770489558936219510E-15 ) ) ;
#11696=CARTESIAN_POINT ( 'NONE',  ( 78.00000000000001421, 0.000000000000000000, 0.000000000000000000 ) ) ;
#11698=CARTESIAN_POINT ( 'NONE',  ( 78.00000000000001421, 0.000000000000000000, 3.309499999999999886 ) ) ;
#11764=DIRECTION ( 'NONE',  ( -1.000000000000000000, -0.000000000000000000, -0.000000000000000000 ) ) ;
#11797=UNCERTAINTY_MEASURE_WITH_UNIT (LENGTH_MEASURE( 1.000000000000000082E-05 ), #22406, 'distance_accuracy_value', 'NONE');
#11805=AXIS2_PLACEMENT_3D ( 'NONE', #9976, #20699, #23252 ) ;
#11824=CIRCLE ( 'NONE', #14542, 6.099999999999999645 ) ;
#11864=LINE ( 'NONE', #11698, #20378 ) ;
#11899=LINE ( 'NONE', #14618, #1984 ) ;
#11922=VECTOR ( 'NONE', #23267, 1000.000000000000000 ) ;
#11941=DIRECTION ( 'NONE',  ( 0.000000000000000000, 0.000000000000000000, 1.000000000000000000 ) ) ;
#12014=EDGE_CURVE ( 'NONE', #4979, #780, #12180, .T. ) ;
#12020=FILL_AREA_STYLE ('',( #32632 ) ) ;
#12102=EDGE_LOOP ( 'NONE', ( #1223, #10275, #2917, #28981, #16693 ) ) ;
#12105=AXIS2_PLACEMENT_3D ( 'NONE', #13817, #11438, #8870 ) ;
#12131=ORIENTED_EDGE ( 'NONE', *, *, #24915, .T. ) ;
#12162=AXIS2_PLACEMENT_3D ( 'NONE', #24572, #19960, #22524 ) ;
#12180=CIRCLE ( 'NONE', #27963, 3.047499999999999876 ) ;
#12227=ORIENTED_EDGE ( 'NONE', *, *, #12276, .F. ) ;
#12276=EDGE_CURVE ( 'NONE', #28362, #2597, #8065, .T. ) ;
#12361=AXIS2_PLACEMENT_3D ( 'NONE', #27890, #9499, #1498 ) ;
#12434=VECTOR ( 'NONE', #26215, 1000.000000000000000 ) ;
#12514=DIRECTION ( 'NONE',  ( -1.000000000000000000, 0.000000000000000000, -0.000000000000000000 ) ) ;
#12530=CARTESIAN_POINT ( 'NONE',  ( 0.000000000000000000, -1.759474945355388176, -3.047499999999998099 ) ) ;
#12565=LINE ( 'NONE', #15116, #15080 ) ;
#12602=EDGE_CURVE ( 'NONE', #13425, #10071, #23183, .T. ) ;
#12688=DIRECTION ( 'NONE',  ( 0.000000000000000000, 0.000000000000000000, 1.000000000000000000 ) ) ;
#12804=CARTESIAN_POINT ( 'NONE',  ( 4.000000000000000000, 3.518949890710768802, -4.770489558936219510E-15 ) ) ;
#12857=ORIENTED_EDGE ( 'NONE', *, *, #22521, .T. ) ;
#12858=CARTESIAN_POINT ( 'NONE',  ( 0.3999999999999975797, 0.000000000000000000, 0.000000000000000000 ) ) ;
#12863=EDGE_CURVE ( 'NONE', #13425, #32876, #16504, .T. ) ;
#12937=ORIENTED_EDGE ( 'NONE', *, *, #2955, .T. ) ;
#12940=LINE ( 'NONE', #21104, #30126 ) ;
#12945=PRODUCT_DEFINITION ( 'UNKNOWN', '', #27867, #14186 ) ;
#12946=EDGE_CURVE ( 'NONE', #30536, #30105, #30473, .T. ) ;
#12978=LINE ( 'NONE', #12804, #21952 ) ;
#13013=ORIENTED_EDGE ( 'NONE', *, *, #25144, .F. ) ;
#13026=CARTESIAN_POINT ( 'NONE',  ( 8.399999999999998579, 0.000000000000000000, 0.000000000000000000 ) ) ;
#13072=DIRECTION ( 'NONE',  ( -1.000000000000000000, -0.000000000000000000, -0.000000000000000000 ) ) ;
#13147=ORIENTED_EDGE ( 'NONE', *, *, #1826, .F. ) ;
#13174=CARTESIAN_POINT ( 'NONE',  ( 4.000000000000000000, 3.518949890710768802, -4.770489558936219510E-15 ) ) ;
#13185=ORIENTED_EDGE ( 'NONE', *, *, #31480, .T. ) ;
#13310=CYLINDRICAL_SURFACE ( 'NONE', #5334, 4.000000000000000888 ) ;
#13325=DIRECTION ( 'NONE',  ( -1.000000000000000000, -0.000000000000000000, -0.000000000000000000 ) ) ;
#13328=EDGE_CURVE ( 'NONE', #4979, #9657, #26858, .T. ) ;
#13397=CLOSED_SHELL ( 'NONE', ( #30057, #5596, #18940, #15010, #30174, #27037, #17455, #18278, #5799, #24450, #19679, #28701, #14405, #18318, #26847, #9259, #20012, #33275, #10576, #10500, #16465, #7695, #9550, #17050, #4789, #22435, #19596 ) ) ;
#13425=VERTEX_POINT ( 'NONE', #15970 ) ;
#13427=AXIS2_PLACEMENT_3D ( 'NONE', #259, #26469, #16077 ) ;
#13447=AXIS2_PLACEMENT_3D ( 'NONE', #3374, #33184, #19383 ) ;
#13501=EDGE_CURVE ( 'NONE', #24969, #33593, #11864, .T. ) ;
#13529=AXIS2_PLACEMENT_3D ( 'NONE', #3313, #32563, #19624 ) ;
#13666=EDGE_LOOP ( 'NONE', ( #30274, #19808, #7839, #5183 ) ) ;
#13679=DIRECTION ( 'NONE',  ( 0.000000000000000000, 0.000000000000000000, -1.000000000000000000 ) ) ;
#13753=VECTOR ( 'NONE', #22570, 1000.000000000000000 ) ;
#13809=DIRECTION ( 'NONE',  ( 0.000000000000000000, 0.000000000000000000, 1.000000000000000000 ) ) ;
#13817=CARTESIAN_POINT ( 'NONE',  ( 8.399999999999998579, 0.000000000000000000, 0.000000000000000000 ) ) ;
#13820=DIRECTION ( 'NONE',  ( 0.000000000000000000, -1.224646799147353207E-16, 1.000000000000000000 ) ) ;
#13837=ORIENTED_EDGE ( 'NONE', *, *, #19865, .F. ) ;
#13857=CARTESIAN_POINT ( 'NONE',  ( 4.000000000000000000, 1.759474945355380404, -3.047500000000001652 ) ) ;
#13902=( NAMED_UNIT ( * ) PLANE_ANGLE_UNIT ( ) SI_UNIT ( $, .RADIAN. ) );
#13922=EDGE_CURVE ( 'NONE', #5750, #4673, #15343, .T. ) ;
#13928=ORIENTED_EDGE ( 'NONE', *, *, #12602, .T. ) ;
#13967=EDGE_CURVE ( 'NONE', #30536, #24528, #26760, .T. ) ;
#14054=EDGE_LOOP ( 'NONE', ( #9169, #15775, #12857, #23577 ) ) ;
#14180=LINE ( 'NONE', #22689, #30278 ) ;
#14186=PRODUCT_DEFINITION_CONTEXT ( 'detailed design', #4855, 'design' ) ;
#14188=AXIS2_PLACEMENT_3D ( 'NONE', #14957, #9335, #14446 ) ;
#14336=PLANE ( 'NONE',  #17516 ) ;
#14372=AXIS2_PLACEMENT_3D ( 'NONE', #5795, #16695, #13809 ) ;
#14380=CARTESIAN_POINT ( 'NONE',  ( 4.000000000000000000, -1.759474945355381958, 3.047500000000001208 ) ) ;
#14404=EDGE_LOOP ( 'NONE', ( #19552, #16194, #32392, #30522 ) ) ;
#14405=ADVANCED_FACE ( 'NONE', ( #373 ), #25155, .F. ) ;
#14446=DIRECTION ( 'NONE',  ( 0.000000000000000000, 0.000000000000000000, 1.000000000000000000 ) ) ;
#14483=CARTESIAN_POINT ( 'NONE',  ( 78.00000000000001421, 0.000000000000000000, 0.000000000000000000 ) ) ;
#14542=AXIS2_PLACEMENT_3D ( 'NONE', #23298, #13072, #30800 ) ;
#14613=VECTOR ( 'NONE', #26176, 1000.000000000000000 ) ;
#14618=CARTESIAN_POINT ( 'NONE',  ( -31.74999999999995737, 4.898587196589413815E-16, -4.000000000000000888 ) ) ;
#14641=AXIS2_PLACEMENT_3D ( 'NONE', #13174, #7225, #22894 ) ;
#14722=PLANE ( 'NONE',  #7229 ) ;
#14813=PLANE ( 'NONE',  #19798 ) ;
#14833=DIRECTION ( 'NONE',  ( 1.000000000000000000, 0.000000000000000000, 0.000000000000000000 ) ) ;
#14841=CARTESIAN_POINT ( 'NONE',  ( 4.000000000000000000, 0.000000000000000000, 0.000000000000000000 ) ) ;
#14843=ORIENTED_EDGE ( 'NONE', *, *, #28282, .T. ) ;
#14885=ORIENTED_EDGE ( 'NONE', *, *, #31107, .F. ) ;
#14957=CARTESIAN_POINT ( 'NONE',  ( 0.000000000000000000, 0.000000000000000000, 0.000000000000000000 ) ) ;
#15010=ADVANCED_FACE ( 'NONE', ( #9132 ), #25725, .T. ) ;
#15014=LINE ( 'NONE', #19956, #32568 ) ;
#15061=FACE_OUTER_BOUND ( 'NONE', #25886, .T. ) ;
#15070=ORIENTED_EDGE ( 'NONE', *, *, #27364, .F. ) ;
#15080=VECTOR ( 'NONE', #28582, 1000.000000000000000 ) ;
#15105=VERTEX_POINT ( 'NONE', #24641 ) ;
#15116=CARTESIAN_POINT ( 'NONE',  ( 4.000000000000000000, -3.518949890710769246, 3.686287386450715076E-15 ) ) ;
#15119=PLANE ( 'NONE',  #24905 ) ;
#15127=VECTOR ( 'NONE', #28983, 1000.000000000000000 ) ;
#15198=ORIENTED_EDGE ( 'NONE', *, *, #12602, .F. ) ;
#15322=DIRECTION ( 'NONE',  ( -0.7071067811865314745, 8.659560562355128841E-17, -0.7071067811865635599 ) ) ;
#15343=CIRCLE ( 'NONE', #28935, 4.000000000000000888 ) ;
#15442=DIRECTION ( 'NONE',  ( 1.000000000000000000, 0.000000000000000000, 0.000000000000000000 ) ) ;
#15514=DIRECTION ( 'NONE',  ( -1.000000000000000000, -0.000000000000000000, -0.000000000000000000 ) ) ;
#15562=VERTEX_POINT ( 'NONE', #22383 ) ;
#15625=CARTESIAN_POINT ( 'NONE',  ( 4.000000000000000000, 1.759474945355380404, -3.047500000000001652 ) ) ;
#15626=CARTESIAN_POINT ( 'NONE',  ( 4.000000000000000000, 0.000000000000000000, 3.047499999999999876 ) ) ;
#15729=FACE_OUTER_BOUND ( 'NONE', #28895, .T. ) ;
#15775=ORIENTED_EDGE ( 'NONE', *, *, #13967, .T. ) ;
#15783=CARTESIAN_POINT ( 'NONE',  ( 0.3999999999999975797, 0.000000000000000000, 0.000000000000000000 ) ) ;
#15847=FACE_OUTER_BOUND ( 'NONE', #6175, .T. ) ;
#15920=VECTOR ( 'NONE', #18174, 1000.000000000000000 ) ;
#15937=CARTESIAN_POINT ( 'NONE',  ( 4.000000000000000000, 3.732111120401558708E-16, -3.047499999999999876 ) ) ;
#15944=ORIENTED_EDGE ( 'NONE', *, *, #12863, .F. ) ;
#15970=CARTESIAN_POINT ( 'NONE',  ( 0.000000000000000000, 3.518949890710768802, -4.770489558936219510E-15 ) ) ;
#15998=ORIENTED_EDGE ( 'NONE', *, *, #13922, .F. ) ;
#16055=EDGE_CURVE ( 'NONE', #5750, #5337, #29571, .T. ) ;
#16077=DIRECTION ( 'NONE',  ( 0.000000000000000000, 0.4999999999999995004, -0.8660254037844389297 ) ) ;
#16142=ORIENTED_EDGE ( 'NONE', *, *, #4170, .F. ) ;
#16189=AXIS2_PLACEMENT_3D ( 'NONE', #7802, #28585, #5237 ) ;
#16191=CIRCLE ( 'NONE', #21641, 3.309499999999999886 ) ;
#16194=ORIENTED_EDGE ( 'NONE', *, *, #12946, .T. ) ;
#16196=EDGE_CURVE ( 'NONE', #24528, #30536, #18633, .T. ) ;
#16266=CARTESIAN_POINT ( 'NONE',  ( 4.000000000000000000, -1.759474945355381958, 3.047500000000001208 ) ) ;
#16277=FACE_OUTER_BOUND ( 'NONE', #783, .T. ) ;
#16314=ORIENTED_EDGE ( 'NONE', *, *, #30373, .F. ) ;
#16373=EDGE_CURVE ( 'NONE', #28318, #780, #12978, .T. ) ;
#16465=ADVANCED_FACE ( 'NONE', ( #28315 ), #37, .F. ) ;
#16483=LINE ( 'NONE', #5599, #12434 ) ;
#16504=LINE ( 'NONE', #3561, #7303 ) ;
#16567=ORIENTED_EDGE ( 'NONE', *, *, #7049, .T. ) ;
#16613=ORIENTED_EDGE ( 'NONE', *, *, #30340, .F. ) ;
#16620=SHAPE_REPRESENTATION_RELATIONSHIP ( 'NONE' , 'NONE' ,  #32622, #33198 ) ;
#16693=ORIENTED_EDGE ( 'NONE', *, *, #23945, .T. ) ;
#16695=DIRECTION ( 'NONE',  ( -1.000000000000000000, -0.000000000000000000, -0.000000000000000000 ) ) ;
#16957=SURFACE_STYLE_FILL_AREA ( #12020 ) ;
#17026=EDGE_CURVE ( 'NONE', #6222, #27878, #2502, .T. ) ;
#17050=ADVANCED_FACE ( 'NONE', ( #2832 ), #5216, .F. ) ;
#17056=DIRECTION ( 'NONE',  ( 0.000000000000000000, 0.000000000000000000, -1.000000000000000000 ) ) ;
#17096=VECTOR ( 'NONE', #22653, 1000.000000000000000 ) ;
#17254=DIRECTION ( 'NONE',  ( 1.000000000000000000, 0.000000000000000000, 0.000000000000000000 ) ) ;
#17372=ORIENTED_EDGE ( 'NONE', *, *, #13328, .T. ) ;
#17455=ADVANCED_FACE ( 'NONE', ( #32777, #15061 ), #14722, .T. ) ;
#17516=AXIS2_PLACEMENT_3D ( 'NONE', #22165, #14833, #17056 ) ;
#17574=DIRECTION ( 'NONE',  ( 1.000000000000000000, 0.000000000000000000, 0.000000000000000000 ) ) ;
#17641=DIRECTION ( 'NONE',  ( -1.000000000000000000, -0.000000000000000000, -0.000000000000000000 ) ) ;
#17711=ORIENTED_EDGE ( 'NONE', *, *, #21633, .T. ) ;
#17746=DIRECTION ( 'NONE',  ( 0.000000000000000000, -0.5000000000000013323, -0.8660254037844379305 ) ) ;
#17829=ORIENTED_EDGE ( 'NONE', *, *, #18686, .F. ) ;
#17836=VERTEX_POINT ( 'NONE', #2967 ) ;
#17854=AXIS2_PLACEMENT_3D ( 'NONE', #1582, #19305, #9076 ) ;
#17954=CARTESIAN_POINT ( 'NONE',  ( 4.000000000000000000, 1.759474945355380404, -3.047500000000001652 ) ) ;
#17982=CARTESIAN_POINT ( 'NONE',  ( 4.000000000000000000, -3.518949890710769246, 3.686287386450715076E-15 ) ) ;
#18097=EDGE_LOOP ( 'NONE', ( #13928, #16142, #24274, #22639, #31378 ) ) ;
#18124=AXIS2_PLACEMENT_3D ( 'NONE', #11696, #27857, #19531 ) ;
#18142=ORIENTED_EDGE ( 'NONE', *, *, #26173, .T. ) ;
#18163=CARTESIAN_POINT ( 'NONE',  ( 0.000000000000000000, -1.759474945355381958, 3.047500000000001208 ) ) ;
#18174=DIRECTION ( 'NONE',  ( -0.5000000000000061062, 1.060575238724902601E-16, -0.8660254037844351549 ) ) ;
#18244=CARTESIAN_POINT ( 'NONE',  ( 77.30950000000004252, 4.898587196589413815E-16, -4.000000000000000000 ) ) ;
#18278=ADVANCED_FACE ( 'NONE', ( #9408 ), #25248, .T. ) ;
#18318=ADVANCED_FACE ( 'NONE', ( #16277 ), #5611, .T. ) ;
#18367=CARTESIAN_POINT ( 'NONE',  ( 8.000000000000000000, 5.388445916248354013E-16, 4.400000000000001243 ) ) ;
#18438=EDGE_LOOP ( 'NONE', ( #15944, #14885, #18886, #17372, #691 ) ) ;
#18448=VECTOR ( 'NONE', #1206, 1000.000000000000000 ) ;
#18480=ORIENTED_EDGE ( 'NONE', *, *, #1000, .F. ) ;
#18493=CARTESIAN_POINT ( 'NONE',  ( 4.000000000000000000, -1.759474945355381958, 3.047500000000001208 ) ) ;
#18512=CARTESIAN_POINT ( 'NONE',  ( 4.000000000000000000, 1.759474945355380404, -3.047500000000001652 ) ) ;
#18518=DIRECTION ( 'NONE',  ( 0.000000000000000000, 0.000000000000000000, 1.000000000000000000 ) ) ;
#18579=DIRECTION ( 'NONE',  ( 0.000000000000000000, 0.000000000000000000, -1.000000000000000000 ) ) ;
#18583=LINE ( 'NONE', #525, #26800 ) ;
#18633=CIRCLE ( 'NONE', #12162, 6.500000000000000000 ) ;
#18686=EDGE_CURVE ( 'NONE', #9657, #32876, #9969, .T. ) ;
#18886=ORIENTED_EDGE ( 'NONE', *, *, #24347, .T. ) ;
#18940=ADVANCED_FACE ( 'NONE', ( #10970 ), #29569, .F. ) ;
#18984=AXIS2_PLACEMENT_3D ( 'NONE', #33418, #30187, #2244 ) ;
#19305=DIRECTION ( 'NONE',  ( 1.000000000000000000, 0.000000000000000000, 0.000000000000000000 ) ) ;
#19327=DIRECTION ( 'NONE',  ( -0.000000000000000000, 1.478898702612462246E-15, 1.000000000000000000 ) ) ;
#19383=DIRECTION ( 'NONE',  ( 0.000000000000000000, 1.224646799147353207E-16, 1.000000000000000000 ) ) ;
#19421=CARTESIAN_POINT ( 'NONE',  ( 4.000000000000000000, 0.000000000000000000, 0.000000000000000000 ) ) ;
#19424=CIRCLE ( 'NONE', #30303, 3.309499999999999886 ) ;
#19531=DIRECTION ( 'NONE',  ( 0.000000000000000000, 0.000000000000000000, 1.000000000000000000 ) ) ;
#19552=ORIENTED_EDGE ( 'NONE', *, *, #16196, .T. ) ;
#19564=LINE ( 'NONE', #4054, #19953 ) ;
#19569=DIRECTION ( 'NONE',  ( 0.000000000000000000, 0.000000000000000000, 1.000000000000000000 ) ) ;
#19577=LINE ( 'NONE', #33200, #6997 ) ;
#19596=ADVANCED_FACE ( 'NONE', ( #29478 ), #24708, .F. ) ;
#19624=DIRECTION ( 'NONE',  ( 0.000000000000000000, 0.000000000000000000, 1.000000000000000000 ) ) ;
#19679=ADVANCED_FACE ( 'NONE', ( #3913 ), #27425, .T. ) ;
#19773=CARTESIAN_POINT ( 'NONE',  ( 0.000000000000000000, -1.759474945355381958, 3.047500000000001208 ) ) ;
#19798=AXIS2_PLACEMENT_3D ( 'NONE', #25208, #4085, #20266 ) ;
#19804=DIRECTION ( 'NONE',  ( 0.000000000000000000, 0.000000000000000000, 1.000000000000000000 ) ) ;
#19808=ORIENTED_EDGE ( 'NONE', *, *, #9591, .T. ) ;
#19826=DIRECTION ( 'NONE',  ( -1.000000000000000000, -0.000000000000000000, -0.000000000000000000 ) ) ;
#19865=EDGE_CURVE ( 'NONE', #27878, #15105, #10567, .T. ) ;
#19895=CYLINDRICAL_SURFACE ( 'NONE', #32464, 6.500000000000000000 ) ;
#19924=LINE ( 'NONE', #9883, #17096 ) ;
#19952=EDGE_CURVE ( 'NONE', #32104, #33208, #19924, .T. ) ;
#19953=VECTOR ( 'NONE', #13325, 1000.000000000000000 ) ;
#19956=CARTESIAN_POINT ( 'NONE',  ( 0.000000000000000000, 1.759474945355380404, -3.047500000000001652 ) ) ;
#19960=DIRECTION ( 'NONE',  ( -1.000000000000000000, -0.000000000000000000, -0.000000000000000000 ) ) ;
#20012=ADVANCED_FACE ( 'NONE', ( #4425 ), #14813, .T. ) ;
#20192=CARTESIAN_POINT ( 'NONE',  ( 4.000000000000000000, -1.759474945355388176, -3.047499999999998099 ) ) ;
#20214=EDGE_CURVE ( 'NONE', #2588, #5010, #12940, .T. ) ;
#20216=DIRECTION ( 'NONE',  ( -1.000000000000000000, -0.000000000000000000, -0.000000000000000000 ) ) ;
#20217=ORIENTED_EDGE ( 'NONE', *, *, #30373, .T. ) ;
#20266=DIRECTION ( 'NONE',  ( 0.000000000000000000, 0.5000000000000009992, 0.8660254037844380415 ) ) ;
#20289=DIRECTION ( 'NONE',  ( -1.000000000000000000, -0.000000000000000000, -0.000000000000000000 ) ) ;
#20321=( GEOMETRIC_REPRESENTATION_CONTEXT ( 3 ) GLOBAL_UNCERTAINTY_ASSIGNED_CONTEXT ( ( #11797 ) ) GLOBAL_UNIT_ASSIGNED_CONTEXT ( ( #22406, #6408, #4019 ) ) REPRESENTATION_CONTEXT ( 'NONE', 'WORKASPACE' ) );
#20334=AXIS2_PLACEMENT_3D ( 'NONE', #13026, #10481, #31421 ) ;
#20359=DIRECTION ( 'NONE',  ( 0.000000000000000000, 0.000000000000000000, 1.000000000000000000 ) ) ;
#20378=VECTOR ( 'NONE', #4186, 1000.000000000000000 ) ;
#20559=ORIENTED_EDGE ( 'NONE', *, *, #29077, .F. ) ;
#20697=CARTESIAN_POINT ( 'NONE',  ( 8.399999999999998579, 4.898587196589413815E-16, -4.000000000000000888 ) ) ;
#20699=DIRECTION ( 'NONE',  ( -1.000000000000000000, -0.000000000000000000, -0.000000000000000000 ) ) ;
#20728=CARTESIAN_POINT ( 'NONE',  ( 0.3999999999999975797, 0.000000000000000000, 0.000000000000000000 ) ) ;
#20773=ORIENTED_EDGE ( 'NONE', *, *, #19952, .F. ) ;
#20900=DIRECTION ( 'NONE',  ( 0.000000000000000000, 0.000000000000000000, 1.000000000000000000 ) ) ;
#21036=AXIS2_PLACEMENT_3D ( 'NONE', #8896, #15442, #29016 ) ;
#21104=CARTESIAN_POINT ( 'NONE',  ( 78.00000000000001421, 4.052968581778165278E-16, -3.309499999999999886 ) ) ;
#21144=CARTESIAN_POINT ( 'NONE',  ( 4.000000000000000000, -3.518949890710769246, 3.686287386450715076E-15 ) ) ;
#21307=DIRECTION ( 'NONE',  ( 0.000000000000000000, 0.000000000000000000, 1.000000000000000000 ) ) ;
#21323=CARTESIAN_POINT ( 'NONE',  ( 4.000000000000000000, -1.759474945355381958, 3.047500000000001208 ) ) ;
#21367=VERTEX_POINT ( 'NONE', #22872 ) ;
#21372=FACE_OUTER_BOUND ( 'NONE', #27421, .T. ) ;
#21376=ORIENTED_EDGE ( 'NONE', *, *, #1992, .T. ) ;
#21481=ORIENTED_EDGE ( 'NONE', *, *, #24347, .F. ) ;
#21490=CARTESIAN_POINT ( 'NONE',  ( 0.3999999999999975797, 7.470345474798854293E-16, -6.099999999999999645 ) ) ;
#21530=CARTESIAN_POINT ( 'NONE',  ( 4.000000000000000000, -1.759474945355381958, 3.047500000000001208 ) ) ;
#21558=UNCERTAINTY_MEASURE_WITH_UNIT (LENGTH_MEASURE( 1.000000000000000082E-05 ), #32821, 'distance_accuracy_value', 'NONE');
#21633=EDGE_CURVE ( 'NONE', #5010, #33593, #23189, .T. ) ;
#21641=AXIS2_PLACEMENT_3D ( 'NONE', #25714, #2556, #4936 ) ;
#21695=AXIS2_PLACEMENT_3D ( 'NONE', #21490, #29330, #13820 ) ;
#21922=AXIS2_PLACEMENT_3D ( 'NONE', #4119, #22528, #19804 ) ;
#21952=VECTOR ( 'NONE', #17746, 1000.000000000000000 ) ;
#21963=DIRECTION ( 'NONE',  ( -1.000000000000000000, -0.000000000000000000, -0.000000000000000000 ) ) ;
#22118=FACE_OUTER_BOUND ( 'NONE', #14404, .T. ) ;
#22165=CARTESIAN_POINT ( 'NONE',  ( 4.000000000000000000, 3.518949890710768802, -4.770489558936219510E-15 ) ) ;
#22266=SURFACE_SIDE_STYLE ('',( #6254 ) ) ;
#22383=CARTESIAN_POINT ( 'NONE',  ( 0.000000000000000000, 7.715274834628324392E-16, -6.099999999999999645 ) ) ;
#22406=( LENGTH_UNIT ( ) NAMED_UNIT ( * ) SI_UNIT ( .MILLI., .METRE. ) );
#22435=ADVANCED_FACE ( 'NONE', ( #24231 ), #32230, .F. ) ;
#22482=ORIENTED_EDGE ( 'NONE', *, *, #26207, .F. ) ;
#22521=EDGE_CURVE ( 'NONE', #24528, #17836, #14180, .T. ) ;
#22524=DIRECTION ( 'NONE',  ( 0.000000000000000000, 0.000000000000000000, 1.000000000000000000 ) ) ;
#22528=DIRECTION ( 'NONE',  ( -1.000000000000000000, -0.000000000000000000, -0.000000000000000000 ) ) ;
#22540=DIRECTION ( 'NONE',  ( -1.000000000000000000, -0.000000000000000000, -0.000000000000000000 ) ) ;
#22570=DIRECTION ( 'NONE',  ( -1.000000000000000000, -0.000000000000000000, -0.000000000000000000 ) ) ;
#22639=ORIENTED_EDGE ( 'NONE', *, *, #16373, .F. ) ;
#22653=DIRECTION ( 'NONE',  ( 0.000000000000000000, 0.4999999999999990563, -0.8660254037844391517 ) ) ;
#22683=DIRECTION ( 'NONE',  ( 0.000000000000000000, 0.000000000000000000, 1.000000000000000000 ) ) ;
#22685=ORIENTED_EDGE ( 'NONE', *, *, #16373, .T. ) ;
#22689=CARTESIAN_POINT ( 'NONE',  ( -31.74999999999995737, 0.000000000000000000, 6.500000000000000000 ) ) ;
#22746=AXIS2_PLACEMENT_3D ( 'NONE', #12858, #9622, #12688 ) ;
#22872=CARTESIAN_POINT ( 'NONE',  ( 4.000000000000000000, 4.506943796211476502E-15, 3.047499999999998543 ) ) ;
#22894=DIRECTION ( 'NONE',  ( 0.000000000000000000, 0.000000000000000000, -1.000000000000000000 ) ) ;
#22976=CARTESIAN_POINT ( 'NONE',  ( 0.000000000000000000, 1.759474945355386399, 3.047499999999995879 ) ) ;
#23013=CARTESIAN_POINT ( 'NONE',  ( 0.000000000000000000, 3.518949890710768802, -4.770489558936219510E-15 ) ) ;
#23074=ORIENTED_EDGE ( 'NONE', *, *, #19952, .T. ) ;
#23077=CARTESIAN_POINT ( 'NONE',  ( 4.000000000000000000, 1.759474945355386399, 3.047499999999995879 ) ) ;
#23101=VECTOR ( 'NONE', #29251, 1000.000000000000114 ) ;
#23183=LINE ( 'NONE', #23013, #5659 ) ;
#23189=CIRCLE ( 'NONE', #7970, 4.000000000000000000 ) ;
#23252=DIRECTION ( 'NONE',  ( 0.000000000000000000, 0.000000000000000000, -1.000000000000000000 ) ) ;
#23267=DIRECTION ( 'NONE',  ( 0.000000000000000000, 1.000000000000000000, -1.478898702612462246E-15 ) ) ;
#23298=CARTESIAN_POINT ( 'NONE',  ( 0.000000000000000000, 0.000000000000000000, 0.000000000000000000 ) ) ;
#23495=ORIENTED_EDGE ( 'NONE', *, *, #1139, .T. ) ;
#23506=CIRCLE ( 'NONE', #27314, 4.000000000000000000 ) ;
#23507=CARTESIAN_POINT ( 'NONE',  ( 78.00000000000001421, 4.475777889183788807E-16, -3.309499999999999886 ) ) ;
#23577=ORIENTED_EDGE ( 'NONE', *, *, #26207, .T. ) ;
#23587=( GEOMETRIC_REPRESENTATION_CONTEXT ( 3 ) GLOBAL_UNCERTAINTY_ASSIGNED_CONTEXT ( ( #6346 ) ) GLOBAL_UNIT_ASSIGNED_CONTEXT ( ( #32798, #13902, #11353 ) ) REPRESENTATION_CONTEXT ( 'NONE', 'WORKASPACE' ) );
#23590=DIRECTION ( 'NONE',  ( 1.000000000000000000, 0.000000000000000000, 0.000000000000000000 ) ) ;
#23615=CARTESIAN_POINT ( 'NONE',  ( 4.000000000000000000, 3.518949890710768802, -4.770489558936219510E-15 ) ) ;
#23704=MANIFOLD_SOLID_BREP ( 'Hex', #13397 ) ;
#23829=VECTOR ( 'NONE', #1451, 1000.000000000000114 ) ;
#23844=CARTESIAN_POINT ( 'NONE',  ( 8.000000000000000000, 0.000000000000000000, -4.400000000000001243 ) ) ;
#23945=EDGE_CURVE ( 'NONE', #780, #27878, #33044, .T. ) ;
#24040=AXIS2_PLACEMENT_3D ( 'NONE', #32585, #22540, #7041 ) ;
#24055=VERTEX_POINT ( 'NONE', #18512 ) ;
#24168=ORIENTED_EDGE ( 'NONE', *, *, #1139, .F. ) ;
#24231=FACE_OUTER_BOUND ( 'NONE', #30790, .T. ) ;
#24274=ORIENTED_EDGE ( 'NONE', *, *, #25576, .F. ) ;
#24347=EDGE_CURVE ( 'NONE', #28318, #4979, #27340, .T. ) ;
#24421=ORIENTED_EDGE ( 'NONE', *, *, #32608, .T. ) ;
#24450=ADVANCED_FACE ( 'NONE', ( #27003 ), #13310, .T. ) ;
#24465=SURFACE_STYLE_USAGE ( .BOTH. , #32126 ) ;
#24528=VERTEX_POINT ( 'NONE', #30753 ) ;
#24572=CARTESIAN_POINT ( 'NONE',  ( 8.000000000000000000, 0.000000000000000000, 0.000000000000000000 ) ) ;
#24589=ORIENTED_EDGE ( 'NONE', *, *, #4877, .F. ) ;
#24641=CARTESIAN_POINT ( 'NONE',  ( 4.000000000000000000, -2.639212418033078489, -1.523749999999997273 ) ) ;
#24688=DIRECTION ( 'NONE',  ( 0.000000000000000000, -0.4999999999999995004, 0.8660254037844389297 ) ) ;
#24708=CONICAL_SURFACE ( 'NONE', #14372, 3.047499999999999876, 1.047197551196590748 ) ;
#24711=CARTESIAN_POINT ( 'NONE',  ( 78.00000000000001421, 0.000000000000000000, 0.000000000000000000 ) ) ;
#24836=ORIENTED_EDGE ( 'NONE', *, *, #6032, .F. ) ;
#24861=ORIENTED_EDGE ( 'NONE', *, *, #814, .F. ) ;
#24896=CARTESIAN_POINT ( 'NONE',  ( 4.000000000000000000, 0.000000000000000000, 0.000000000000000000 ) ) ;
#24905=AXIS2_PLACEMENT_3D ( 'NONE', #15625, #26027, #2699 ) ;
#24915=EDGE_CURVE ( 'NONE', #2597, #32104, #864, .T. ) ;
#24967=AXIS2_PLACEMENT_3D ( 'NONE', #14841, #25239, #22683 ) ;
#24969=VERTEX_POINT ( 'NONE', #25207 ) ;
#25036=ORIENTED_EDGE ( 'NONE', *, *, #1000, .T. ) ;
#25044=ORIENTED_EDGE ( 'NONE', *, *, #16055, .T. ) ;
#25070=FACE_OUTER_BOUND ( 'NONE', #1583, .T. ) ;
#25144=EDGE_CURVE ( 'NONE', #24969, #2588, #16191, .T. ) ;
#25155=TOROIDAL_SURFACE ( 'NONE', #12105, 4.400000000000001243, 0.4000000000000000222 ) ;
#25207=CARTESIAN_POINT ( 'NONE',  ( 78.00000000000001421, 0.000000000000000000, 3.309499999999999886 ) ) ;
#25208=CARTESIAN_POINT ( 'NONE',  ( 4.000000000000000000, -1.759474945355381958, 3.047500000000001208 ) ) ;
#25239=DIRECTION ( 'NONE',  ( -1.000000000000000000, -0.000000000000000000, -0.000000000000000000 ) ) ;
#25248=CYLINDRICAL_SURFACE ( 'NONE', #21922, 6.500000000000000000 ) ;
#25253=ORIENTED_EDGE ( 'NONE', *, *, #12276, .T. ) ;
#25258=ORIENTED_EDGE ( 'NONE', *, *, #27364, .T. ) ;
#25299=ORIENTED_EDGE ( 'NONE', *, *, #32414, .F. ) ;
#25385=CARTESIAN_POINT ( 'NONE',  ( 4.000000000000000000, 1.759474945355386399, 3.047499999999995879 ) ) ;
#25456=CARTESIAN_POINT ( 'NONE',  ( 0.000000000000000000, 0.000000000000000000, 0.000000000000000000 ) ) ;
#25462=CARTESIAN_POINT ( 'NONE',  ( -31.74999999999995737, 0.000000000000000000, 0.000000000000000000 ) ) ;
#25515=CIRCLE ( 'NONE', #21695, 0.4000000000000001887 ) ;
#25576=EDGE_CURVE ( 'NONE', #780, #24055, #16483, .T. ) ;
#25579=CYLINDRICAL_SURFACE ( 'NONE', #18984, 4.000000000000000888 ) ;
#25675=ORIENTED_EDGE ( 'NONE', *, *, #32214, .F. ) ;
#25714=CARTESIAN_POINT ( 'NONE',  ( 78.00000000000001421, 0.000000000000000000, 0.000000000000000000 ) ) ;
#25725=CONICAL_SURFACE ( 'NONE', #18124, 3.309499999999999886, 0.7853981633974710386 ) ;
#25737=CARTESIAN_POINT ( 'NONE',  ( 77.30950000000004252, 0.000000000000000000, 0.000000000000000000 ) ) ;
#25752=ORIENTED_EDGE ( 'NONE', *, *, #6049, .F. ) ;
#25780=VECTOR ( 'NONE', #29499, 1000.000000000000000 ) ;
#25784=LINE ( 'NONE', #17954, #1169 ) ;
#25790=AXIS2_PLACEMENT_3D ( 'NONE', #31045, #17574, #28644 ) ;
#25883=EDGE_LOOP ( 'NONE', ( #33507, #17711, #24421, #30318 ) ) ;
#25886=EDGE_LOOP ( 'NONE', ( #12937, #4934 ) ) ;
#25921=EDGE_LOOP ( 'NONE', ( #8987, #7537, #4974 ) ) ;
#26027=DIRECTION ( 'NONE',  ( 0.000000000000000000, -9.859324684083082301E-16, -1.000000000000000000 ) ) ;
#26173=EDGE_CURVE ( 'NONE', #6985, #28362, #26346, .T. ) ;
#26176=DIRECTION ( 'NONE',  ( 0.000000000000000000, -0.5000000000000009992, -0.8660254037844380415 ) ) ;
#26207=EDGE_CURVE ( 'NONE', #17836, #30105, #1560, .T. ) ;
#26215=DIRECTION ( 'NONE',  ( 0.000000000000000000, -0.5000000000000013323, -0.8660254037844379305 ) ) ;
#26236=CARTESIAN_POINT ( 'NONE',  ( 78.00000000000001421, 3.309499999999999886, 0.000000000000000000 ) ) ;
#26244=CARTESIAN_POINT ( 'NONE',  ( 0.000000000000000000, 0.000000000000000000, 6.099999999999999645 ) ) ;
#26346=LINE ( 'NONE', #31467, #14613 ) ;
#26414=ORIENTED_EDGE ( 'NONE', *, *, #2071, .F. ) ;
#26440=DIRECTION ( 'NONE',  ( -1.000000000000000000, -0.000000000000000000, -0.000000000000000000 ) ) ;
#26469=DIRECTION ( 'NONE',  ( 0.000000000000000000, -0.8660254037844389297, -0.4999999999999995004 ) ) ;
#26666=VERTEX_POINT ( 'NONE', #1786 ) ;
#26747=ORIENTED_EDGE ( 'NONE', *, *, #7049, .F. ) ;
#26760=CIRCLE ( 'NONE', #24040, 6.500000000000000000 ) ;
#26790=EDGE_CURVE ( 'NONE', #6298, #5337, #9077, .T. ) ;
#26800=VECTOR ( 'NONE', #10917, 1000.000000000000000 ) ;
#26847=ADVANCED_FACE ( 'NONE', ( #29370 ), #31267, .T. ) ;
#26858=LINE ( 'NONE', #8308, #23101 ) ;
#27003=FACE_OUTER_BOUND ( 'NONE', #25883, .T. ) ;
#27035=AXIS2_PLACEMENT_3D ( 'NONE', #16266, #19327, #27167 ) ;
#27037=ADVANCED_FACE ( 'NONE', ( #22118 ), #19895, .T. ) ;
#27144=LINE ( 'NONE', #13857, #27643 ) ;
#27161=EDGE_LOOP ( 'NONE', ( #25036, #5226 ) ) ;
#27167=DIRECTION ( 'NONE',  ( 0.000000000000000000, -1.000000000000000000, 1.478898702612462246E-15 ) ) ;
#27176=VERTEX_POINT ( 'NONE', #10661 ) ;
#27233=CARTESIAN_POINT ( 'NONE',  ( -31.74999999999995737, 0.000000000000000000, 0.000000000000000000 ) ) ;
#27239=DIRECTION ( 'NONE',  ( 0.000000000000000000, 1.000000000000000000, -1.478898702612462246E-15 ) ) ;
#27243=LINE ( 'NONE', #9190, #2353 ) ;
#27314=AXIS2_PLACEMENT_3D ( 'NONE', #25737, #15514, #31356 ) ;
#27319=CARTESIAN_POINT ( 'NONE',  ( 77.30950000000004252, 0.000000000000000000, 0.000000000000000000 ) ) ;
#27340=LINE ( 'NONE', #27509, #23829 ) ;
#27352=PRESENTATION_STYLE_ASSIGNMENT (( #24465 ) ) ;
#27364=EDGE_CURVE ( 'NONE', #6985, #27176, #31920, .T. ) ;
#27373=( NAMED_UNIT ( * ) SI_UNIT ( $, .STERADIAN. ) SOLID_ANGLE_UNIT ( ) );
#27421=EDGE_LOOP ( 'NONE', ( #1363, #32205, #7875, #20217, #14843 ) ) ;
#27425=CONICAL_SURFACE ( 'NONE', #10035, 3.309499999999999886, 0.7853981633974710386 ) ;
#27471=EDGE_CURVE ( 'NONE', #21367, #9657, #5857, .T. ) ;
#27477=DIRECTION ( 'NONE',  ( 0.000000000000000000, 0.000000000000000000, -1.000000000000000000 ) ) ;
#27509=CARTESIAN_POINT ( 'NONE',  ( 4.000000000000000000, 3.518949890710768802, -4.770489558936219510E-15 ) ) ;
#27538=( NAMED_UNIT ( * ) PLANE_ANGLE_UNIT ( ) SI_UNIT ( $, .RADIAN. ) );
#27597=CIRCLE ( 'NONE', #13447, 0.4000000000000001887 ) ;
#27631=AXIS2_PLACEMENT_3D ( 'NONE', #24896, #20289, #1719 ) ;
#27643=VECTOR ( 'NONE', #3967, 1000.000000000000000 ) ;
#27674=DIRECTION ( 'NONE',  ( 0.000000000000000000, 0.000000000000000000, 1.000000000000000000 ) ) ;
#27783=CARTESIAN_POINT ( 'NONE',  ( 4.000000000000000000, -2.639212418033075380, 1.523750000000003268 ) ) ;
#27792=DIRECTION ( 'NONE',  ( 0.000000000000000000, -1.000000000000000000, 0.000000000000000000 ) ) ;
#27834=DIRECTION ( 'NONE',  ( -0.000000000000000000, 0.000000000000000000, 1.000000000000000000 ) ) ;
#27857=DIRECTION ( 'NONE',  ( -1.000000000000000000, -0.000000000000000000, -0.000000000000000000 ) ) ;
#27867=PRODUCT_DEFINITION_FORMATION_WITH_SPECIFIED_SOURCE ( 'ANY', '', #30091, .NOT_KNOWN. ) ;
#27878=VERTEX_POINT ( 'NONE', #2453 ) ;
#27890=CARTESIAN_POINT ( 'NONE',  ( 8.000000000000000000, 0.000000000000000000, 0.000000000000000000 ) ) ;
#27945=DIRECTION ( 'NONE',  ( 0.000000000000000000, -0.5000000000000009992, -0.8660254037844380415 ) ) ;
#27963=AXIS2_PLACEMENT_3D ( 'NONE', #31675, #8669, #3222 ) ;
#28003=PLANE ( 'NONE',  #14641 ) ;
#28016=ORIENTED_EDGE ( 'NONE', *, *, #32608, .F. ) ;
#28051=DIRECTION ( 'NONE',  ( 0.000000000000000000, 0.000000000000000000, 1.000000000000000000 ) ) ;
#28282=EDGE_CURVE ( 'NONE', #28362, #21367, #29266, .T. ) ;
#28315=FACE_OUTER_BOUND ( 'NONE', #32293, .T. ) ;
#28318=VERTEX_POINT ( 'NONE', #33241 ) ;
#28362=VERTEX_POINT ( 'NONE', #27783 ) ;
#28447=AXIS2_PLACEMENT_3D ( 'NONE', #6115, #29463, #29301 ) ;
#28454=ORIENTED_EDGE ( 'NONE', *, *, #4877, .T. ) ;
#28465=SHAPE_DEFINITION_REPRESENTATION ( #6987, #32622 ) ;
#28477=CIRCLE ( 'NONE', #4508, 0.4000000000000001887 ) ;
#28582=DIRECTION ( 'NONE',  ( 0.000000000000000000, 0.4999999999999990563, -0.8660254037844391517 ) ) ;
#28585=DIRECTION ( 'NONE',  ( 0.000000000000000000, 0.8660254037844379305, -0.5000000000000013323 ) ) ;
#28644=DIRECTION ( 'NONE',  ( 0.000000000000000000, 0.000000000000000000, -1.000000000000000000 ) ) ;
#28701=ADVANCED_FACE ( 'NONE', ( #15847 ), #7528, .T. ) ;
#28812=ORIENTED_EDGE ( 'NONE', *, *, #2955, .F. ) ;
#28820=ORIENTED_EDGE ( 'NONE', *, *, #12863, .T. ) ;
#28877=LINE ( 'NONE', #18163, #11922 ) ;
#28895=EDGE_LOOP ( 'NONE', ( #5839, #12227, #16314 ) ) ;
#28935=AXIS2_PLACEMENT_3D ( 'NONE', #9765, #17254, #27477 ) ;
#28981=ORIENTED_EDGE ( 'NONE', *, *, #12014, .T. ) ;
#28983=DIRECTION ( 'NONE',  ( -1.000000000000000000, -0.000000000000000000, -0.000000000000000000 ) ) ;
#29016=DIRECTION ( 'NONE',  ( 0.000000000000000000, 0.000000000000000000, -1.000000000000000000 ) ) ;
#29062=ORIENTED_EDGE ( 'NONE', *, *, #32201, .T. ) ;
#29077=EDGE_CURVE ( 'NONE', #6985, #21367, #19577, .T. ) ;
#29214=CARTESIAN_POINT ( 'NONE',  ( 0.3999999999999975797, 7.960204194457795477E-16, -6.500000000000000000 ) ) ;
#29251=DIRECTION ( 'NONE',  ( 0.000000000000000000, -0.4999999999999995004, 0.8660254037844389297 ) ) ;
#29266=CIRCLE ( 'NONE', #27631, 3.047499999999999876 ) ;
#29301=DIRECTION ( 'NONE',  ( 0.000000000000000000, 0.000000000000000000, 1.000000000000000000 ) ) ;
#29330=DIRECTION ( 'NONE',  ( -0.000000000000000000, 1.000000000000000000, 1.224646799147353207E-16 ) ) ;
#29370=FACE_OUTER_BOUND ( 'NONE', #18438, .T. ) ;
#29440=CARTESIAN_POINT ( 'NONE',  ( 4.000000000000000000, 2.639212418033074492, -1.523750000000004157 ) ) ;
#29463=DIRECTION ( 'NONE',  ( 1.000000000000000000, 0.000000000000000000, 0.000000000000000000 ) ) ;
#29478=FACE_OUTER_BOUND ( 'NONE', #12102, .T. ) ;
#29499=DIRECTION ( 'NONE',  ( 0.000000000000000000, -0.5000000000000009992, -0.8660254037844380415 ) ) ;
#29569=TOROIDAL_SURFACE ( 'NONE', #20334, 4.400000000000001243, 0.4000000000000000222 ) ;
#29571=CIRCLE ( 'NONE', #2928, 0.4000000000000001887 ) ;
#29826=DIRECTION ( 'NONE',  ( -1.000000000000000000, -0.000000000000000000, -0.000000000000000000 ) ) ;
#29836=DIRECTION ( 'NONE',  ( 0.000000000000000000, 0.000000000000000000, -1.000000000000000000 ) ) ;
#29882=APPLICATION_CONTEXT ( 'automotive_design' ) ;
#30057=ADVANCED_FACE ( 'NONE', ( #21372 ), #4292, .F. ) ;
#30058=ORIENTED_EDGE ( 'NONE', *, *, #13922, .T. ) ;
#30091=PRODUCT ( 'socket head cap screw_iso_ISO 4762 M8 x 70 - 28N', 'socket head cap screw_iso_ISO 4762 M8 x 70 - 28N', '', ( #7686 ) ) ;
#30105=VERTEX_POINT ( 'NONE', #29214 ) ;
#30126=VECTOR ( 'NONE', #15322, 1000.000000000000000 ) ;
#30147=EDGE_LOOP ( 'NONE', ( #20773, #9702, #21376, #23495, #9919 ) ) ;
#30174=ADVANCED_FACE ( 'NONE', ( #25070 ), #25579, .T. ) ;
#30187=DIRECTION ( 'NONE',  ( -1.000000000000000000, -0.000000000000000000, -0.000000000000000000 ) ) ;
#30274=ORIENTED_EDGE ( 'NONE', *, *, #20214, .F. ) ;
#30278=VECTOR ( 'NONE', #6517, 1000.000000000000000 ) ;
#30299=CARTESIAN_POINT ( 'NONE',  ( -31.74999999999995737, 7.960204194457795477E-16, -6.500000000000000000 ) ) ;
#30303=AXIS2_PLACEMENT_3D ( 'NONE', #14483, #11764, #30502 ) ;
#30318=ORIENTED_EDGE ( 'NONE', *, *, #6049, .T. ) ;
#30323=ORIENTED_EDGE ( 'NONE', *, *, #26790, .F. ) ;
#30340=EDGE_CURVE ( 'NONE', #10071, #33208, #15014, .T. ) ;
#30353=DIRECTION ( 'NONE',  ( 0.000000000000000000, -1.000000000000000000, 9.859324684083082301E-16 ) ) ;
#30358=CIRCLE ( 'NONE', #17854, 4.000000000000000888 ) ;
#30373=EDGE_CURVE ( 'NONE', #15105, #28362, #31510, .T. ) ;
#30473=LINE ( 'NONE', #30299, #4024 ) ;
#30489=VERTEX_POINT ( 'NONE', #26244 ) ;
#30502=DIRECTION ( 'NONE',  ( 0.000000000000000000, 0.000000000000000000, 1.000000000000000000 ) ) ;
#30522=ORIENTED_EDGE ( 'NONE', *, *, #22521, .F. ) ;
#30536=VERTEX_POINT ( 'NONE', #30871 ) ;
#30582=EDGE_LOOP ( 'NONE', ( #16567, #17829, #1764, #20559, #25258 ) ) ;
#30659=ORIENTED_EDGE ( 'NONE', *, *, #4170, .T. ) ;
#30744=ORIENTED_EDGE ( 'NONE', *, *, #20214, .T. ) ;
#30753=CARTESIAN_POINT ( 'NONE',  ( 8.000000000000000000, 0.000000000000000000, 6.500000000000000000 ) ) ;
#30763=DIRECTION ( 'NONE',  ( 0.000000000000000000, -0.4999999999999990563, 0.8660254037844391517 ) ) ;
#30790=EDGE_LOOP ( 'NONE', ( #1648, #4383, #3087 ) ) ;
#30800=DIRECTION ( 'NONE',  ( 0.000000000000000000, 0.000000000000000000, 1.000000000000000000 ) ) ;
#30871=CARTESIAN_POINT ( 'NONE',  ( 8.000000000000000000, 7.960204194457795477E-16, -6.500000000000000000 ) ) ;
#30890=VECTOR ( 'NONE', #1427, 1000.000000000000000 ) ;
#30936=FACE_OUTER_BOUND ( 'NONE', #30147, .T. ) ;
#31045=CARTESIAN_POINT ( 'NONE',  ( 4.000000000000000000, 3.518949890710768802, -4.770489558936219510E-15 ) ) ;
#31107=EDGE_CURVE ( 'NONE', #28318, #13425, #19564, .T. ) ;
#31267=PLANE ( 'NONE',  #13427 ) ;
#31310=LINE ( 'NONE', #15626, #31909 ) ;
#31356=DIRECTION ( 'NONE',  ( 0.000000000000000000, 0.000000000000000000, 1.000000000000000000 ) ) ;
#31378=ORIENTED_EDGE ( 'NONE', *, *, #31107, .T. ) ;
#31421=DIRECTION ( 'NONE',  ( 0.000000000000000000, 0.000000000000000000, -1.000000000000000000 ) ) ;
#31467=CARTESIAN_POINT ( 'NONE',  ( 4.000000000000000000, -1.759474945355381958, 3.047500000000001208 ) ) ;
#31480=EDGE_CURVE ( 'NONE', #5010, #5750, #11899, .T. ) ;
#31510=CIRCLE ( 'NONE', #24967, 3.047499999999999876 ) ;
#31529=CARTESIAN_POINT ( 'NONE',  ( 0.000000000000000000, -3.518949890710769246, 3.686287386450715076E-15 ) ) ;
#31628=EDGE_CURVE ( 'NONE', #6222, #21367, #31310, .T. ) ;
#31675=CARTESIAN_POINT ( 'NONE',  ( 4.000000000000000000, 0.000000000000000000, 0.000000000000000000 ) ) ;
#31697=ORIENTED_EDGE ( 'NONE', *, *, #13967, .F. ) ;
#31874=LINE ( 'NONE', #11112, #18448 ) ;
#31909=VECTOR ( 'NONE', #2854, 1000.000000000000000 ) ;
#31914=CARTESIAN_POINT ( 'NONE',  ( 77.30950000000004252, 0.000000000000000000, 4.000000000000000000 ) ) ;
#31920=LINE ( 'NONE', #21530, #955 ) ;
#32104=VERTEX_POINT ( 'NONE', #31529 ) ;
#32126=SURFACE_SIDE_STYLE ('',( #16957 ) ) ;
#32201=EDGE_CURVE ( 'NONE', #17836, #30489, #28477, .T. ) ;
#32205=ORIENTED_EDGE ( 'NONE', *, *, #17026, .T. ) ;
#32214=EDGE_CURVE ( 'NONE', #30105, #17836, #32781, .T. ) ;
#32230=PLANE ( 'NONE',  #21036 ) ;
#32270=PLANE ( 'NONE',  #27035 ) ;
#32293=EDGE_LOOP ( 'NONE', ( #3496, #24168, #13837 ) ) ;
#32392=ORIENTED_EDGE ( 'NONE', *, *, #32214, .T. ) ;
#32414=EDGE_CURVE ( 'NONE', #24055, #27878, #18583, .T. ) ;
#32464=AXIS2_PLACEMENT_3D ( 'NONE', #27233, #9179, #19569 ) ;
#32563=DIRECTION ( 'NONE',  ( -1.000000000000000000, -0.000000000000000000, -0.000000000000000000 ) ) ;
#32568=VECTOR ( 'NONE', #30353, 1000.000000000000000 ) ;
#32585=CARTESIAN_POINT ( 'NONE',  ( 8.000000000000000000, 0.000000000000000000, 0.000000000000000000 ) ) ;
#32608=EDGE_CURVE ( 'NONE', #33593, #4673, #27243, .T. ) ;
#32622=SHAPE_REPRESENTATION ( 'socket head cap screw_iso_ISO 4762 M8 x 70 - 28N', ( #2404 ), #20321 ) ;
#32632=FILL_AREA_STYLE_COLOUR ( '', #9995 ) ;
#32771=AXIS2_PLACEMENT_3D ( 'NONE', #23615, #10845, #7783 ) ;
#32777=FACE_BOUND ( 'NONE', #2628, .T. ) ;
#32779=CARTESIAN_POINT ( 'NONE',  ( 4.000000000000000000, 0.000000000000000000, 0.000000000000000000 ) ) ;
#32781=CIRCLE ( 'NONE', #28447, 6.500000000000000000 ) ;
#32798=( LENGTH_UNIT ( ) NAMED_UNIT ( * ) SI_UNIT ( .MILLI., .METRE. ) );
#32821=( LENGTH_UNIT ( ) NAMED_UNIT ( * ) SI_UNIT ( .MILLI., .METRE. ) );
#32876=VERTEX_POINT ( 'NONE', #22976 ) ;
#32881=ORIENTED_EDGE ( 'NONE', *, *, #32201, .F. ) ;
#32953=DIRECTION ( 'NONE',  ( -1.000000000000000000, -0.000000000000000000, -0.000000000000000000 ) ) ;
#33044=CIRCLE ( 'NONE', #8566, 3.047499999999999876 ) ;
#33121=ORIENTED_EDGE ( 'NONE', *, *, #13501, .F. ) ;
#33149=LINE ( 'NONE', #20192, #5382 ) ;
#33184=DIRECTION ( 'NONE',  ( 0.000000000000000000, 1.000000000000000000, -1.224646799147353207E-16 ) ) ;
#33198=ADVANCED_BREP_SHAPE_REPRESENTATION ( '', ( #23704, #2404 ), #20321 ) ;
#33200=CARTESIAN_POINT ( 'NONE',  ( 4.000000000000000000, -1.759474945355381958, 3.047500000000001208 ) ) ;
#33208=VERTEX_POINT ( 'NONE', #12530 ) ;
#33241=CARTESIAN_POINT ( 'NONE',  ( 4.000000000000000000, 3.518949890710768802, -4.770489558936219510E-15 ) ) ;
#33275=ADVANCED_FACE ( 'NONE', ( #30936 ), #5522, .T. ) ;
#33356=FACE_OUTER_BOUND ( 'NONE', #18097, .T. ) ;
#33418=CARTESIAN_POINT ( 'NONE',  ( -31.74999999999995737, 0.000000000000000000, 0.000000000000000000 ) ) ;
#33507=ORIENTED_EDGE ( 'NONE', *, *, #31480, .F. ) ;
#33593=VERTEX_POINT ( 'NONE', #31914 ) ;
ENDSEC;
END-ISO-10303-21;
